ISO-10303-21;
HEADER;
/* Generated by software containing ST-Developer
 * from STEP Tools, Inc. (www.steptools.com) 
 */

FILE_DESCRIPTION(
/* description */ ('Crank-driven oscillating fan base (mechanism only)'),

/* implementation_level */ '2;1');

FILE_NAME(
/* name */ 'Upper pin keeper (1).step',
/* time_stamp */ '2026-10-28T03:25:00-07:00',
/* author */ (''),
/* organization */ (''),
/* preprocessor_version */ 'ST-DEVELOPER v20.2',
/* originating_system */ 'Autodesk Translation Framework v15.17.0.0',
/* authorisation */ '');

FILE_SCHEMA (('AUTOMOTIVE_DESIGN { 1 0 10303 214 3 1 1 }'));
ENDSEC;

DATA;
#10=MECHANICAL_DESIGN_GEOMETRIC_PRESENTATION_REPRESENTATION('',(#478),#11916);
#390=SHAPE_REPRESENTATION_RELATIONSHIP('SRR','None',#12117,#430);
#430=ADVANCED_BREP_SHAPE_REPRESENTATION('',(#525),#11908);
#478=STYLED_ITEM('',(#12375),#525);
#525=MANIFOLD_SOLID_BREP('Body1',#6109);
#679=FACE_BOUND('',#1724,.T.);
#680=FACE_BOUND('',#1726,.T.);
#845=PLANE('',#7247);
#846=PLANE('',#7248);
#1197=FACE_OUTER_BOUND('',#1721,.T.);
#1198=FACE_OUTER_BOUND('',#1722,.T.);
#1199=FACE_OUTER_BOUND('',#1723,.T.);
#1200=FACE_OUTER_BOUND('',#1725,.T.);
#1721=EDGE_LOOP('',(#5304,#5305,#5306,#5307));
#1722=EDGE_LOOP('',(#5308,#5309,#5310,#5311));
#1723=EDGE_LOOP('',(#5312));
#1724=EDGE_LOOP('',(#5313));
#1725=EDGE_LOOP('',(#5314));
#1726=EDGE_LOOP('',(#5315));
#2048=LINE('',#11496,#2381);
#2049=LINE('',#11502,#2382);
#2381=VECTOR('',#9029,0.225);
#2382=VECTOR('',#9036,0.5);
#2791=CIRCLE('',#7242,0.225);
#2792=CIRCLE('',#7243,0.225);
#2793=CIRCLE('',#7245,0.5);
#2794=CIRCLE('',#7246,0.5);
#3251=VERTEX_POINT('',#11493);
#3252=VERTEX_POINT('',#11495);
#3253=VERTEX_POINT('',#11499);
#3254=VERTEX_POINT('',#11501);
#3947=EDGE_CURVE('',#3251,#3251,#2791,.T.);
#3948=EDGE_CURVE('',#3251,#3252,#2048,.T.);
#3949=EDGE_CURVE('',#3252,#3252,#2792,.T.);
#3950=EDGE_CURVE('',#3253,#3253,#2793,.T.);
#3951=EDGE_CURVE('',#3253,#3254,#2049,.T.);
#3952=EDGE_CURVE('',#3254,#3254,#2794,.T.);
#5304=ORIENTED_EDGE('',*,*,#3947,.F.);
#5305=ORIENTED_EDGE('',*,*,#3948,.T.);
#5306=ORIENTED_EDGE('',*,*,#3949,.T.);
#5307=ORIENTED_EDGE('',*,*,#3948,.F.);
#5308=ORIENTED_EDGE('',*,*,#3950,.F.);
#5309=ORIENTED_EDGE('',*,*,#3951,.T.);
#5310=ORIENTED_EDGE('',*,*,#3952,.T.);
#5311=ORIENTED_EDGE('',*,*,#3951,.F.);
#5312=ORIENTED_EDGE('',*,*,#3950,.T.);
#5313=ORIENTED_EDGE('',*,*,#3947,.T.);
#5314=ORIENTED_EDGE('',*,*,#3952,.F.);
#5315=ORIENTED_EDGE('',*,*,#3949,.F.);
#5677=CYLINDRICAL_SURFACE('',#7241,0.225);
#5678=CYLINDRICAL_SURFACE('',#7244,0.5);
#6003=ADVANCED_FACE('',(#1197),#5677,.F.);
#6004=ADVANCED_FACE('',(#1198),#5678,.T.);
#6005=ADVANCED_FACE('',(#1199,#679),#845,.T.);
#6006=ADVANCED_FACE('',(#1200,#680),#846,.F.);
#6109=CLOSED_SHELL('',(#6003,#6004,#6005,#6006));
#7240=AXIS2_PLACEMENT_3D('',#11491,#9023,#9024);
#7241=AXIS2_PLACEMENT_3D('',#11492,#9025,#9026);
#7242=AXIS2_PLACEMENT_3D('',#11494,#9027,#9028);
#7243=AXIS2_PLACEMENT_3D('',#11497,#9030,#9031);
#7244=AXIS2_PLACEMENT_3D('',#11498,#9032,#9033);
#7245=AXIS2_PLACEMENT_3D('',#11500,#9034,#9035);
#7246=AXIS2_PLACEMENT_3D('',#11503,#9037,#9038);
#7247=AXIS2_PLACEMENT_3D('',#11504,#9039,#9040);
#7248=AXIS2_PLACEMENT_3D('',#11505,#9041,#9042);
#9023=DIRECTION('axis',(0.,0.,1.));
#9024=DIRECTION('refdir',(1.,0.,0.));
#9025=DIRECTION('center_axis',(0.,0.,1.));
#9026=DIRECTION('ref_axis',(1.,0.,0.));
#9027=DIRECTION('center_axis',(0.,0.,-1.));
#9028=DIRECTION('ref_axis',(1.,0.,0.));
#9029=DIRECTION('',(0.,0.,-1.));
#9030=DIRECTION('center_axis',(0.,0.,-1.));
#9031=DIRECTION('ref_axis',(1.,0.,0.));
#9032=DIRECTION('center_axis',(0.,0.,1.));
#9033=DIRECTION('ref_axis',(1.,0.,0.));
#9034=DIRECTION('center_axis',(0.,0.,1.));
#9035=DIRECTION('ref_axis',(1.,0.,0.));
#9036=DIRECTION('',(0.,0.,-1.));
#9037=DIRECTION('center_axis',(0.,0.,1.));
#9038=DIRECTION('ref_axis',(1.,0.,0.));
#9039=DIRECTION('center_axis',(0.,0.,1.));
#9040=DIRECTION('ref_axis',(1.,0.,0.));
#9041=DIRECTION('center_axis',(0.,0.,1.));
#9042=DIRECTION('ref_axis',(1.,0.,0.));
#11491=CARTESIAN_POINT('',(0.,0.,0.));
#11492=CARTESIAN_POINT('Origin',(8.,4.,9.6));
#11493=CARTESIAN_POINT('',(7.775,4.,9.8));
#11494=CARTESIAN_POINT('Origin',(8.,4.,9.8));
#11495=CARTESIAN_POINT('',(7.775,4.,9.6));
#11496=CARTESIAN_POINT('',(7.775,4.,9.6));
#11497=CARTESIAN_POINT('Origin',(8.,4.,9.6));
#11498=CARTESIAN_POINT('Origin',(8.,4.,9.6));
#11499=CARTESIAN_POINT('',(7.5,4.,9.8));
#11500=CARTESIAN_POINT('Origin',(8.,4.,9.8));
#11501=CARTESIAN_POINT('',(7.5,4.,9.6));
#11502=CARTESIAN_POINT('',(7.5,4.,9.6));
#11503=CARTESIAN_POINT('Origin',(8.,4.,9.6));
#11504=CARTESIAN_POINT('Origin',(8.,4.,9.8));
#11505=CARTESIAN_POINT('Origin',(8.,4.,9.6));
#11861=UNCERTAINTY_MEASURE_WITH_UNIT(LENGTH_MEASURE(0.001),#11917,
'DISTANCE_ACCURACY_VALUE',
'Maximum model space distance between geometric entities at asserted c
onnectivities');
#11869=UNCERTAINTY_MEASURE_WITH_UNIT(LENGTH_MEASURE(0.001),#11917,
'DISTANCE_ACCURACY_VALUE',
'Maximum model space distance between geometric entities at asserted c
onnectivities');
#11908=(
GEOMETRIC_REPRESENTATION_CONTEXT(3)
GLOBAL_UNCERTAINTY_ASSIGNED_CONTEXT((#11861))
GLOBAL_UNIT_ASSIGNED_CONTEXT((#11917,#11919,#11920))
REPRESENTATION_CONTEXT('','3D')
);
#11916=(
GEOMETRIC_REPRESENTATION_CONTEXT(3)
GLOBAL_UNCERTAINTY_ASSIGNED_CONTEXT((#11869))
GLOBAL_UNIT_ASSIGNED_CONTEXT((#11917,#11919,#11920))
REPRESENTATION_CONTEXT('','3D')
);
#11917=(
LENGTH_UNIT()
NAMED_UNIT(*)
SI_UNIT(.CENTI.,.METRE.)
);
#11919=(
NAMED_UNIT(*)
PLANE_ANGLE_UNIT()
SI_UNIT($,.RADIAN.)
);
#11920=(
NAMED_UNIT(*)
SI_UNIT($,.STERADIAN.)
SOLID_ANGLE_UNIT()
);
#11959=SHAPE_DEFINITION_REPRESENTATION(#12010,#12117);
#12010=PRODUCT_DEFINITION_SHAPE('',$,#12164);
#12117=SHAPE_REPRESENTATION('',(#7240),#11908);
#12125=PRODUCT_DEFINITION_CONTEXT('part definition',#12265,'design');
#12164=PRODUCT_DEFINITION('Upper pin keeper (1)','Upper pin keeper (1)',#12210,
#12125);
#12210=PRODUCT_DEFINITION_FORMATION('',$,#12305);
#12265=APPLICATION_CONTEXT(
'Core Data for Automotive Mechanical Design Process');
#12266=PRODUCT_CONTEXT('part definition',#12265,'mechanical');
#12305=PRODUCT('Upper pin keeper (1)','Upper pin keeper (1)',
'Upper pin keeper (1)',(#12266));
#12369=COLOUR_RGB('Grey',0.48,0.52,0.57);
#12370=FILL_AREA_STYLE_COLOUR('',#12369);
#12371=FILL_AREA_STYLE('',(#12370));
#12372=SURFACE_STYLE_FILL_AREA(#12371);
#12373=SURFACE_SIDE_STYLE('',(#12372));
#12374=SURFACE_STYLE_USAGE(.BOTH.,#12373);
#12375=PRESENTATION_STYLE_ASSIGNMENT((#12374));
ENDSEC;
END-ISO-10303-21;
